ISO-10303-21;
HEADER;
/* Generated by software containing ST-Developer
 * from STEP Tools, Inc. (www.steptools.com) 
 */

FILE_DESCRIPTION(
/* description */ ('Turntable on roller ring'),
/* implementation_level */ '2;1');

FILE_NAME(
/* name */ 'Outer race retainer (2).step',
/* time_stamp */ '2026-10-28T03:23:59-07:00',
/* author */ (''),
/* organization */ (''),
/* preprocessor_version */ 'ST-DEVELOPER v20.2',
/* originating_system */ 'Autodesk Translation Framework v15.17.0.0',
/* authorisation */ '');

FILE_SCHEMA (('AUTOMOTIVE_DESIGN { 1 0 10303 214 3 1 1 }'));
ENDSEC;

DATA;
#10=MECHANICAL_DESIGN_GEOMETRIC_PRESENTATION_REPRESENTATION('',(#668),#16281);
#549=SHAPE_REPRESENTATION_RELATIONSHIP('SRR','None',#16571,#604);
#604=ADVANCED_BREP_SHAPE_REPRESENTATION('',(#736),#16265);
#668=STYLED_ITEM('',(#16932),#736);
#736=MANIFOLD_SOLID_BREP('Body1',#8413);
#965=FACE_BOUND('',#2388,.T.);
#966=FACE_BOUND('',#2390,.T.);
#1217=PLANE('',#9973);
#1218=PLANE('',#9974);
#1672=FACE_OUTER_BOUND('',#2385,.T.);
#1673=FACE_OUTER_BOUND('',#2386,.T.);
#1674=FACE_OUTER_BOUND('',#2387,.T.);
#1675=FACE_OUTER_BOUND('',#2389,.T.);
#2385=EDGE_LOOP('',(#7361,#7362,#7363,#7364));
#2386=EDGE_LOOP('',(#7365,#7366,#7367,#7368));
#2387=EDGE_LOOP('',(#7369));
#2388=EDGE_LOOP('',(#7370));
#2389=EDGE_LOOP('',(#7371));
#2390=EDGE_LOOP('',(#7372));
#2944=LINE('',#15415,#3427);
#2945=LINE('',#15421,#3428);
#3427=VECTOR('',#12509,1.1);
#3428=VECTOR('',#12516,1.5);
#3845=CIRCLE('',#9968,1.1);
#3846=CIRCLE('',#9969,1.1);
#3847=CIRCLE('',#9971,1.5);
#3848=CIRCLE('',#9972,1.5);
#4521=VERTEX_POINT('',#15412);
#4522=VERTEX_POINT('',#15414);
#4523=VERTEX_POINT('',#15418);
#4524=VERTEX_POINT('',#15420);
#5491=EDGE_CURVE('',#4521,#4521,#3845,.T.);
#5492=EDGE_CURVE('',#4521,#4522,#2944,.T.);
#5493=EDGE_CURVE('',#4522,#4522,#3846,.T.);
#5494=EDGE_CURVE('',#4523,#4523,#3847,.T.);
#5495=EDGE_CURVE('',#4523,#4524,#2945,.T.);
#5496=EDGE_CURVE('',#4524,#4524,#3848,.T.);
#7361=ORIENTED_EDGE('',*,*,#5491,.F.);
#7362=ORIENTED_EDGE('',*,*,#5492,.T.);
#7363=ORIENTED_EDGE('',*,*,#5493,.T.);
#7364=ORIENTED_EDGE('',*,*,#5492,.F.);
#7365=ORIENTED_EDGE('',*,*,#5494,.F.);
#7366=ORIENTED_EDGE('',*,*,#5495,.T.);
#7367=ORIENTED_EDGE('',*,*,#5496,.T.);
#7368=ORIENTED_EDGE('',*,*,#5495,.F.);
#7369=ORIENTED_EDGE('',*,*,#5494,.T.);
#7370=ORIENTED_EDGE('',*,*,#5491,.T.);
#7371=ORIENTED_EDGE('',*,*,#5496,.F.);
#7372=ORIENTED_EDGE('',*,*,#5493,.F.);
#7825=CYLINDRICAL_SURFACE('',#9967,1.1);
#7826=CYLINDRICAL_SURFACE('',#9970,1.5);
#8275=ADVANCED_FACE('',(#1672),#7825,.F.);
#8276=ADVANCED_FACE('',(#1673),#7826,.T.);
#8277=ADVANCED_FACE('',(#1674,#965),#1217,.T.);
#8278=ADVANCED_FACE('',(#1675,#966),#1218,.F.);
#8413=CLOSED_SHELL('',(#8275,#8276,#8277,#8278));
#9966=AXIS2_PLACEMENT_3D('',#15410,#12503,#12504);
#9967=AXIS2_PLACEMENT_3D('',#15411,#12505,#12506);
#9968=AXIS2_PLACEMENT_3D('',#15413,#12507,#12508);
#9969=AXIS2_PLACEMENT_3D('',#15416,#12510,#12511);
#9970=AXIS2_PLACEMENT_3D('',#15417,#12512,#12513);
#9971=AXIS2_PLACEMENT_3D('',#15419,#12514,#12515);
#9972=AXIS2_PLACEMENT_3D('',#15422,#12517,#12518);
#9973=AXIS2_PLACEMENT_3D('',#15423,#12519,#12520);
#9974=AXIS2_PLACEMENT_3D('',#15424,#12521,#12522);
#12503=DIRECTION('axis',(0.,0.,1.));
#12504=DIRECTION('refdir',(1.,0.,0.));
#12505=DIRECTION('center_axis',(0.,1.,0.));
#12506=DIRECTION('ref_axis',(1.,0.,0.));
#12507=DIRECTION('center_axis',(0.,-1.,0.));
#12508=DIRECTION('ref_axis',(1.,0.,0.));
#12509=DIRECTION('',(0.,-1.,0.));
#12510=DIRECTION('center_axis',(0.,-1.,0.));
#12511=DIRECTION('ref_axis',(1.,0.,0.));
#12512=DIRECTION('center_axis',(0.,1.,0.));
#12513=DIRECTION('ref_axis',(1.,0.,0.));
#12514=DIRECTION('center_axis',(0.,1.,0.));
#12515=DIRECTION('ref_axis',(1.,0.,0.));
#12516=DIRECTION('',(0.,-1.,0.));
#12517=DIRECTION('center_axis',(0.,1.,0.));
#12518=DIRECTION('ref_axis',(1.,0.,0.));
#12519=DIRECTION('center_axis',(0.,1.,0.));
#12520=DIRECTION('ref_axis',(1.,0.,0.));
#12521=DIRECTION('center_axis',(0.,1.,0.));
#12522=DIRECTION('ref_axis',(1.,0.,0.));
#15410=CARTESIAN_POINT('',(0.,0.,0.));
#15411=CARTESIAN_POINT('Origin',(0.,14.35,3.5));
#15412=CARTESIAN_POINT('',(-1.1,14.55,3.5));
#15413=CARTESIAN_POINT('Origin',(0.,14.55,3.5));
#15414=CARTESIAN_POINT('',(-1.1,14.35,3.5));
#15415=CARTESIAN_POINT('',(-1.1,14.35,3.5));
#15416=CARTESIAN_POINT('Origin',(0.,14.35,3.5));
#15417=CARTESIAN_POINT('Origin',(0.,14.35,3.5));
#15418=CARTESIAN_POINT('',(-1.5,14.55,3.5));
#15419=CARTESIAN_POINT('Origin',(0.,14.55,3.5));
#15420=CARTESIAN_POINT('',(-1.5,14.35,3.5));
#15421=CARTESIAN_POINT('',(-1.5,14.35,3.5));
#15422=CARTESIAN_POINT('Origin',(0.,14.35,3.5));
#15423=CARTESIAN_POINT('Origin',(0.,14.55,3.5));
#15424=CARTESIAN_POINT('Origin',(0.,14.35,3.5));
#16196=UNCERTAINTY_MEASURE_WITH_UNIT(LENGTH_MEASURE(0.001),#16282,
'DISTANCE_ACCURACY_VALUE',
'Maximum model space distance between geometric entities at asserted c
onnectivities');
#16212=UNCERTAINTY_MEASURE_WITH_UNIT(LENGTH_MEASURE(0.001),#16282,
'DISTANCE_ACCURACY_VALUE',
'Maximum model space distance between geometric entities at asserted c
onnectivities');
#16265=(
GEOMETRIC_REPRESENTATION_CONTEXT(3)
GLOBAL_UNCERTAINTY_ASSIGNED_CONTEXT((#16196))
GLOBAL_UNIT_ASSIGNED_CONTEXT((#16282,#16284,#16285))
REPRESENTATION_CONTEXT('','3D')
);
#16281=(
GEOMETRIC_REPRESENTATION_CONTEXT(3)
GLOBAL_UNCERTAINTY_ASSIGNED_CONTEXT((#16212))
GLOBAL_UNIT_ASSIGNED_CONTEXT((#16282,#16284,#16285))
REPRESENTATION_CONTEXT('','3D')
);
#16282=(
LENGTH_UNIT()
NAMED_UNIT(*)
SI_UNIT(.CENTI.,.METRE.)
);
#16284=(
NAMED_UNIT(*)
PLANE_ANGLE_UNIT()
SI_UNIT($,.RADIAN.)
);
#16285=(
NAMED_UNIT(*)
SI_UNIT($,.STERADIAN.)
SOLID_ANGLE_UNIT()
);
#16338=SHAPE_DEFINITION_REPRESENTATION(#16472,#16571);
#16472=PRODUCT_DEFINITION_SHAPE('',$,#16640);
#16571=SHAPE_REPRESENTATION('',(#9966),#16265);
#16587=PRODUCT_DEFINITION_CONTEXT('part definition',#16793,'design');
#16640=PRODUCT_DEFINITION('Outer race retainer (2)',
'Outer race retainer (2)',#16708,#16587);
#16708=PRODUCT_DEFINITION_FORMATION('',$,#16847);
#16793=APPLICATION_CONTEXT(
'Core Data for Automotive Mechanical Design Process');
#16794=PRODUCT_CONTEXT('part definition',#16793,'mechanical');
#16847=PRODUCT('Outer race retainer (2)','Outer race retainer (2)',
'Outer race retainer (2)',(#16794));
#16926=COLOUR_RGB('Grey',0.48,0.52,0.57);
#16927=FILL_AREA_STYLE_COLOUR('',#16926);
#16928=FILL_AREA_STYLE('',(#16927));
#16929=SURFACE_STYLE_FILL_AREA(#16928);
#16930=SURFACE_SIDE_STYLE('',(#16929));
#16931=SURFACE_STYLE_USAGE(.BOTH.,#16930);
#16932=PRESENTATION_STYLE_ASSIGNMENT((#16931));
ENDSEC;
END-ISO-10303-21;
